ISO-10303-21;
HEADER;
/* Generated by software containing ST-Developer
 * from STEP Tools, Inc. (www.steptools.com) 
 */

FILE_DESCRIPTION(
/* description */ ('Four-valve pipe header'),
/* implementation_level */ '2;1');

FILE_NAME(
/* name */ 'Flat Washer - M5.step',
/* time_stamp */ '2026-10-29T16:56:19-07:00',
/* author */ (''),
/* organization */ (''),
/* preprocessor_version */ 'ST-DEVELOPER v20.2',
/* originating_system */ 'Autodesk Translation Framework v15.17.0.0',
/* authorisation */ '');

FILE_SCHEMA (('AUTOMOTIVE_DESIGN { 1 0 10303 214 3 1 1 }'));
ENDSEC;

DATA;
#10=MECHANICAL_DESIGN_GEOMETRIC_PRESENTATION_REPRESENTATION('',(#347),#10119);
#269=CONICAL_SURFACE('',#6319,0.275,0.785398163397449);
#295=SHAPE_REPRESENTATION_RELATIONSHIP('SRR','None',#10257,#321);
#321=ADVANCED_BREP_SHAPE_REPRESENTATION('',(#372),#10106);
#347=STYLED_ITEM('',(#10477),#372);
#372=MANIFOLD_SOLID_BREP('Body1',#5594);
#515=FACE_BOUND('',#1383,.T.);
#516=FACE_BOUND('',#1386,.T.);
#658=PLANE('',#6324);
#659=PLANE('',#6328);
#959=FACE_OUTER_BOUND('',#1380,.T.);
#960=FACE_OUTER_BOUND('',#1381,.T.);
#961=FACE_OUTER_BOUND('',#1382,.T.);
#962=FACE_OUTER_BOUND('',#1384,.T.);
#963=FACE_OUTER_BOUND('',#1385,.T.);
#1380=EDGE_LOOP('',(#4669,#4670,#4671,#4672));
#1381=EDGE_LOOP('',(#4673,#4674,#4675,#4676));
#1382=EDGE_LOOP('',(#4677));
#1383=EDGE_LOOP('',(#4678));
#1384=EDGE_LOOP('',(#4679,#4680,#4681,#4682));
#1385=EDGE_LOOP('',(#4683));
#1386=EDGE_LOOP('',(#4684));
#1772=LINE('',#9456,#2190);
#1773=LINE('',#9460,#2191);
#1774=LINE('',#9467,#2192);
#2190=VECTOR('',#7673,0.275);
#2191=VECTOR('',#7678,0.265);
#2192=VECTOR('',#7687,0.5);
#2518=CIRCLE('',#6320,0.285);
#2519=CIRCLE('',#6321,0.265);
#2520=CIRCLE('',#6323,0.265);
#2521=CIRCLE('',#6325,0.5);
#2522=CIRCLE('',#6327,0.5);
#2883=VERTEX_POINT('',#9453);
#2884=VERTEX_POINT('',#9455);
#2885=VERTEX_POINT('',#9459);
#2886=VERTEX_POINT('',#9463);
#2887=VERTEX_POINT('',#9466);
#3501=EDGE_CURVE('',#2883,#2883,#2518,.T.);
#3502=EDGE_CURVE('',#2883,#2884,#1772,.T.);
#3503=EDGE_CURVE('',#2884,#2884,#2519,.T.);
#3504=EDGE_CURVE('',#2884,#2885,#1773,.T.);
#3505=EDGE_CURVE('',#2885,#2885,#2520,.T.);
#3506=EDGE_CURVE('',#2886,#2886,#2521,.T.);
#3507=EDGE_CURVE('',#2886,#2887,#1774,.T.);
#3508=EDGE_CURVE('',#2887,#2887,#2522,.T.);
#4669=ORIENTED_EDGE('',*,*,#3501,.T.);
#4670=ORIENTED_EDGE('',*,*,#3502,.T.);
#4671=ORIENTED_EDGE('',*,*,#3503,.T.);
#4672=ORIENTED_EDGE('',*,*,#3502,.F.);
#4673=ORIENTED_EDGE('',*,*,#3503,.F.);
#4674=ORIENTED_EDGE('',*,*,#3504,.T.);
#4675=ORIENTED_EDGE('',*,*,#3505,.T.);
#4676=ORIENTED_EDGE('',*,*,#3504,.F.);
#4677=ORIENTED_EDGE('',*,*,#3506,.T.);
#4678=ORIENTED_EDGE('',*,*,#3501,.F.);
#4679=ORIENTED_EDGE('',*,*,#3506,.F.);
#4680=ORIENTED_EDGE('',*,*,#3507,.T.);
#4681=ORIENTED_EDGE('',*,*,#3508,.T.);
#4682=ORIENTED_EDGE('',*,*,#3507,.F.);
#4683=ORIENTED_EDGE('',*,*,#3508,.F.);
#4684=ORIENTED_EDGE('',*,*,#3505,.F.);
#5229=CYLINDRICAL_SURFACE('',#6322,0.265);
#5230=CYLINDRICAL_SURFACE('',#6326,0.5);
#5459=ADVANCED_FACE('',(#959),#269,.F.);
#5460=ADVANCED_FACE('',(#960),#5229,.F.);
#5461=ADVANCED_FACE('',(#961,#515),#658,.T.);
#5462=ADVANCED_FACE('',(#962),#5230,.T.);
#5463=ADVANCED_FACE('',(#963,#516),#659,.F.);
#5594=CLOSED_SHELL('',(#5459,#5460,#5461,#5462,#5463));
#6318=AXIS2_PLACEMENT_3D('',#9451,#7667,#7668);
#6319=AXIS2_PLACEMENT_3D('',#9452,#7669,#7670);
#6320=AXIS2_PLACEMENT_3D('',#9454,#7671,#7672);
#6321=AXIS2_PLACEMENT_3D('',#9457,#7674,#7675);
#6322=AXIS2_PLACEMENT_3D('',#9458,#7676,#7677);
#6323=AXIS2_PLACEMENT_3D('',#9461,#7679,#7680);
#6324=AXIS2_PLACEMENT_3D('',#9462,#7681,#7682);
#6325=AXIS2_PLACEMENT_3D('',#9464,#7683,#7684);
#6326=AXIS2_PLACEMENT_3D('',#9465,#7685,#7686);
#6327=AXIS2_PLACEMENT_3D('',#9468,#7688,#7689);
#6328=AXIS2_PLACEMENT_3D('',#9469,#7690,#7691);
#7667=DIRECTION('axis',(0.,0.,1.));
#7668=DIRECTION('refdir',(1.,0.,0.));
#7669=DIRECTION('center_axis',(0.,1.,0.));
#7670=DIRECTION('ref_axis',(1.,0.,0.));
#7671=DIRECTION('center_axis',(0.,1.,0.));
#7672=DIRECTION('ref_axis',(1.,0.,0.));
#7673=DIRECTION('',(0.707106781186548,-0.707106781186547,-8.65956056235494E-17));
#7674=DIRECTION('center_axis',(0.,-1.,0.));
#7675=DIRECTION('ref_axis',(1.,0.,0.));
#7676=DIRECTION('center_axis',(0.,1.,0.));
#7677=DIRECTION('ref_axis',(1.,0.,0.));
#7678=DIRECTION('',(0.,-1.,0.));
#7679=DIRECTION('center_axis',(0.,-1.,0.));
#7680=DIRECTION('ref_axis',(1.,0.,0.));
#7681=DIRECTION('center_axis',(0.,1.,0.));
#7682=DIRECTION('ref_axis',(1.,0.,0.));
#7683=DIRECTION('center_axis',(0.,1.,0.));
#7684=DIRECTION('ref_axis',(1.,0.,0.));
#7685=DIRECTION('center_axis',(0.,1.,0.));
#7686=DIRECTION('ref_axis',(1.,0.,0.));
#7687=DIRECTION('',(0.,-1.,0.));
#7688=DIRECTION('center_axis',(0.,1.,0.));
#7689=DIRECTION('ref_axis',(1.,0.,0.));
#7690=DIRECTION('center_axis',(0.,1.,0.));
#7691=DIRECTION('ref_axis',(1.,0.,0.));
#9451=CARTESIAN_POINT('',(0.,0.,0.));
#9452=CARTESIAN_POINT('Origin',(0.,0.09,0.));
#9453=CARTESIAN_POINT('',(-0.285,0.1,3.49024337756996E-17));
#9454=CARTESIAN_POINT('Origin',(0.,0.1,0.));
#9455=CARTESIAN_POINT('',(-0.265,0.08,-3.24531401774049E-17));
#9456=CARTESIAN_POINT('',(-0.275,0.09,3.36777869765522E-17));
#9457=CARTESIAN_POINT('Origin',(0.,0.08,0.));
#9458=CARTESIAN_POINT('Origin',(0.,0.,0.));
#9459=CARTESIAN_POINT('',(-0.265,0.,3.24531401774049E-17));
#9460=CARTESIAN_POINT('',(-0.265,0.,3.24531401774049E-17));
#9461=CARTESIAN_POINT('Origin',(0.,0.,0.));
#9462=CARTESIAN_POINT('Origin',(0.,0.1,0.));
#9463=CARTESIAN_POINT('',(-0.5,0.1,6.12323399573677E-17));
#9464=CARTESIAN_POINT('Origin',(0.,0.1,0.));
#9465=CARTESIAN_POINT('Origin',(0.,0.,0.));
#9466=CARTESIAN_POINT('',(-0.5,0.,6.12323399573677E-17));
#9467=CARTESIAN_POINT('',(-0.5,0.,6.12323399573677E-17));
#9468=CARTESIAN_POINT('Origin',(0.,0.,0.));
#9469=CARTESIAN_POINT('Origin',(0.,0.,0.));
#10075=UNCERTAINTY_MEASURE_WITH_UNIT(LENGTH_MEASURE(0.001),#10120,
'DISTANCE_ACCURACY_VALUE',
'Maximum model space distance between geometric entities at asserted c
onnectivities');
#10088=UNCERTAINTY_MEASURE_WITH_UNIT(LENGTH_MEASURE(0.001),#10120,
'DISTANCE_ACCURACY_VALUE',
'Maximum model space distance between geometric entities at asserted c
onnectivities');
#10106=(
GEOMETRIC_REPRESENTATION_CONTEXT(3)
GLOBAL_UNCERTAINTY_ASSIGNED_CONTEXT((#10075))
GLOBAL_UNIT_ASSIGNED_CONTEXT((#10120,#10122,#10123))
REPRESENTATION_CONTEXT('','3D')
);
#10119=(
GEOMETRIC_REPRESENTATION_CONTEXT(3)
GLOBAL_UNCERTAINTY_ASSIGNED_CONTEXT((#10088))
GLOBAL_UNIT_ASSIGNED_CONTEXT((#10120,#10122,#10123))
REPRESENTATION_CONTEXT('','3D')
);
#10120=(
LENGTH_UNIT()
NAMED_UNIT(*)
SI_UNIT(.CENTI.,.METRE.)
);
#10122=(
NAMED_UNIT(*)
PLANE_ANGLE_UNIT()
SI_UNIT($,.RADIAN.)
);
#10123=(
NAMED_UNIT(*)
SI_UNIT($,.STERADIAN.)
SOLID_ANGLE_UNIT()
);
#10141=SHAPE_DEFINITION_REPRESENTATION(#10171,#10257);
#10171=PRODUCT_DEFINITION_SHAPE('',$,#10288);
#10257=SHAPE_REPRESENTATION('',(#6318),#10106);
#10270=PRODUCT_DEFINITION_CONTEXT('part definition',#10362,'design');
#10288=PRODUCT_DEFINITION('Flat Washer - M5','Flat Washer - M5',#10318,
#10270);
#10318=PRODUCT_DEFINITION_FORMATION('',$,#10381);
#10362=APPLICATION_CONTEXT(
'Core Data for Automotive Mechanical Design Process');
#10363=PRODUCT_CONTEXT('part definition',#10362,'mechanical');
#10381=PRODUCT('Flat Washer - M5','Flat Washer - M5','Flat Washer - M5',
(#10363));
#10471=COLOUR_RGB('Black',0.12,0.14,0.17);
#10472=FILL_AREA_STYLE_COLOUR('',#10471);
#10473=FILL_AREA_STYLE('',(#10472));
#10474=SURFACE_STYLE_FILL_AREA(#10473);
#10475=SURFACE_SIDE_STYLE('',(#10474));
#10476=SURFACE_STYLE_USAGE(.BOTH.,#10475);
#10477=PRESENTATION_STYLE_ASSIGNMENT((#10476));
ENDSEC;
END-ISO-10303-21;
